ISO-10303-21;
HEADER;
FILE_DESCRIPTION (('STEP AP214'),
    '1' );
FILE_NAME ('outer cover 1.step',
    '2026-10-23T14:45:25',
    ( '' ),
    ( '' ),
    'SwSTEP 2.0',
    'SolidWorks 2026',
    '' );
FILE_SCHEMA (( 'AUTOMOTIVE_DESIGN' ));
ENDSEC;

DATA;
#6=EDGE_CURVE ( 'NONE', #2459, #3011, #3096, .T. ) ;
#19=CARTESIAN_POINT ( 'NONE',  ( -5.000000000000085265, 24.49489742783176638, 8.000000000000000000 ) ) ;
#30=VERTEX_POINT ( 'NONE', #94 ) ;
#35=DIRECTION ( 'NONE',  ( 1.000000000000000000, 0.000000000000000000, -0.000000000000000000 ) ) ;
#50=CIRCLE ( 'NONE', #4195, 0.2500000000000002220 ) ;
#57=CARTESIAN_POINT ( 'NONE',  ( -23.00000000000000000, 0.000000000000000000, 8.000000000000000000 ) ) ;
#69=ADVANCED_BREP_SHAPE_REPRESENTATION ( '', ( #652, #1336 ), #2338 ) ;
#81=EDGE_CURVE ( 'NONE', #5595, #92, #3920, .T. ) ;
#92=VERTEX_POINT ( 'NONE', #1069 ) ;
#94=CARTESIAN_POINT ( 'NONE',  ( -23.00000000000000000, 0.000000000000000000, 2.000000000000000000 ) ) ;
#99=ORIENTED_EDGE ( 'NONE', *, *, #1510, .T. ) ;
#109=ORIENTED_EDGE ( 'NONE', *, *, #4578, .T. ) ;
#111=CARTESIAN_POINT ( 'NONE',  ( 17.55913978494622896, -14.85518798308249266, 8.000000000000000000 ) ) ;
#125=EDGE_LOOP ( 'NONE', ( #2926, #4809, #268, #1968 ) ) ;
#132=VERTEX_POINT ( 'NONE', #668 ) ;
#134=AXIS2_PLACEMENT_3D ( 'NONE', #4325, #5590, #2673 ) ;
#135=AXIS2_PLACEMENT_3D ( 'NONE', #259, #5439, #1064 ) ;
#141=DIRECTION ( 'NONE',  ( -0.000000000000000000, -0.000000000000000000, -1.000000000000000000 ) ) ;
#148=DIRECTION ( 'NONE',  ( 0.000000000000000000, 0.000000000000000000, -1.000000000000000000 ) ) ;
#150=ORIENTED_EDGE ( 'NONE', *, *, #4696, .T. ) ;
#155=EDGE_CURVE ( 'NONE', #132, #1194, #1259, .T. ) ;
#165=ORIENTED_EDGE ( 'NONE', *, *, #624, .F. ) ;
#171=EDGE_LOOP ( 'NONE', ( #4985, #2532, #4601, #4935, #348, #2849 ) ) ;
#173=DIRECTION ( 'NONE',  ( 1.000000000000000000, 0.000000000000000000, -0.000000000000000000 ) ) ;
#180=DIRECTION ( 'NONE',  ( -0.000000000000000000, -0.000000000000000000, 1.000000000000000000 ) ) ;
#192=EDGE_LOOP ( 'NONE', ( #1018, #4430, #1762, #1166 ) ) ;
#196=ADVANCED_FACE ( 'NONE', ( #1959 ), #1125, .F. ) ;
#205=DIRECTION ( 'NONE',  ( 1.000000000000000000, 0.000000000000000000, 0.000000000000000000 ) ) ;
#229=CARTESIAN_POINT ( 'NONE',  ( 0.000000000000000000, 0.000000000000000000, 8.000000000000000000 ) ) ;
#241=ORIENTED_EDGE ( 'NONE', *, *, #4606, .T. ) ;
#250=AXIS2_PLACEMENT_3D ( 'NONE', #4950, #1491, #1007 ) ;
#251=ADVANCED_FACE ( 'NONE', ( #5066 ), #4211, .F. ) ;
#259=CARTESIAN_POINT ( 'NONE',  ( 17.74999999999999289, -15.01665741768121443, 8.000000000000000000 ) ) ;
#262=CARTESIAN_POINT ( 'NONE',  ( 0.000000000000000000, 0.000000000000000000, 8.000000000000000000 ) ) ;
#268=ORIENTED_EDGE ( 'NONE', *, *, #1278, .T. ) ;
#283=CARTESIAN_POINT ( 'NONE',  ( 0.000000000000000000, 0.000000000000000000, 0.000000000000000000 ) ) ;
#293=LINE ( 'NONE', #4272, #2527 ) ;
#294=ORIENTED_EDGE ( 'NONE', *, *, #155, .F. ) ;
#306=ADVANCED_FACE ( 'NONE', ( #5530 ), #1618, .T. ) ;
#315=ORIENTED_EDGE ( 'NONE', *, *, #1380, .F. ) ;
#348=ORIENTED_EDGE ( 'NONE', *, *, #1101, .F. ) ;
#356=ORIENTED_EDGE ( 'NONE', *, *, #916, .T. ) ;
#362=EDGE_LOOP ( 'NONE', ( #3338, #2305, #826, #2887 ) ) ;
#367=CARTESIAN_POINT ( 'NONE',  ( 17.74999999999999289, -15.01665741768121443, 8.000000000000000000 ) ) ;
#372=ORIENTED_EDGE ( 'NONE', *, *, #2730, .T. ) ;
#374=DIRECTION ( 'NONE',  ( -3.540989467475305966E-16, -1.000000000000000000, 0.000000000000000000 ) ) ;
#384=PRODUCT_DEFINITION_CONTEXT ( 'detailed design', #596, 'design' ) ;
#395=EDGE_CURVE ( 'NONE', #92, #5595, #4012, .T. ) ;
#400=DIRECTION ( 'NONE',  ( -0.000000000000000000, -0.000000000000000000, -1.000000000000000000 ) ) ;
#402=DIRECTION ( 'NONE',  ( -1.000000000000000000, 0.000000000000000000, 0.000000000000000000 ) ) ;
#411=ORIENTED_EDGE ( 'NONE', *, *, #2956, .T. ) ;
#455=CARTESIAN_POINT ( 'NONE',  ( 5.000000000000000000, 5.000000000000022204, 5.000000000000000000 ) ) ;
#459=LINE ( 'NONE', #4920, #1265 ) ;
#461=CARTESIAN_POINT ( 'NONE',  ( -5.000000000000000000, 0.000000000000000000, 2.000000000000000000 ) ) ;
#471=ORIENTED_EDGE ( 'NONE', *, *, #3814, .F. ) ;
#481=ADVANCED_FACE ( 'NONE', ( #4717 ), #2104, .T. ) ;
#493=ORIENTED_EDGE ( 'NONE', *, *, #4312, .F. ) ;
#516=CARTESIAN_POINT ( 'NONE',  ( -5.000000000000076383, 22.44994432064363110, 5.000000000000000000 ) ) ;
#522=LINE ( 'NONE', #2878, #4544 ) ;
#523=CARTESIAN_POINT ( 'NONE',  ( 0.000000000000000000, 0.000000000000000000, 8.000000000000000000 ) ) ;
#524=PLANE ( 'NONE',  #1617 ) ;
#525=VERTEX_POINT ( 'NONE', #4460 ) ;
#569=CARTESIAN_POINT ( 'NONE',  ( 4.999999999999914735, 24.49489742783179835, 8.000000000000000000 ) ) ;
#576=LINE ( 'NONE', #638, #774 ) ;
#577=LINE ( 'NONE', #4896, #1520 ) ;
#586=VERTEX_POINT ( 'NONE', #461 ) ;
#588=AXIS2_PLACEMENT_3D ( 'NONE', #5265, #4773, #1322 ) ;
#596=APPLICATION_CONTEXT ( 'automotive_design' ) ;
#624=EDGE_CURVE ( 'NONE', #2461, #2258, #1720, .T. ) ;
#638=CARTESIAN_POINT ( 'NONE',  ( 23.48484848484848442, -8.570991287109677614, 8.000000000000000000 ) ) ;
#652=MANIFOLD_SOLID_BREP ( 'Fillet1', #3277 ) ;
#662=CARTESIAN_POINT ( 'NONE',  ( 0.000000000000000000, 0.000000000000000000, 4.000000000000000000 ) ) ;
#668=CARTESIAN_POINT ( 'NONE',  ( 2.000000000000000000, 0.000000000000000000, 8.000000000000000000 ) ) ;
#669=FACE_OUTER_BOUND ( 'NONE', #3074, .T. ) ;
#674=LINE ( 'NONE', #4556, #1058 ) ;
#707=DIRECTION ( 'NONE',  ( 0.000000000000000000, 0.000000000000000000, -1.000000000000000000 ) ) ;
#710=VECTOR ( 'NONE', #902, 1000.000000000000000 ) ;
#711=ORIENTED_EDGE ( 'NONE', *, *, #4312, .T. ) ;
#725=DIRECTION ( 'NONE',  ( -0.000000000000000000, -0.000000000000000000, 1.000000000000000000 ) ) ;
#744=DIRECTION ( 'NONE',  ( -1.000000000000000000, 0.000000000000000000, 0.000000000000000000 ) ) ;
#746=FILL_AREA_STYLE ('',( #1584 ) ) ;
#756=CARTESIAN_POINT ( 'NONE',  ( 25.00000000000000000, 3.061616997868383043E-15, 0.000000000000000000 ) ) ;
#757=EDGE_LOOP ( 'NONE', ( #4197, #5327, #4355, #3268, #3669, #1822, #2688 ) ) ;
#768=CYLINDRICAL_SURFACE ( 'NONE', #3356, 25.00000000000000000 ) ;
#769=AXIS2_PLACEMENT_3D ( 'NONE', #4923, #2711, #4495 ) ;
#774=VECTOR ( 'NONE', #2388, 1000.000000000000000 ) ;
#779=LINE ( 'NONE', #2042, #2167 ) ;
#795=DIRECTION ( 'NONE',  ( 0.000000000000000000, 0.000000000000000000, 1.000000000000000000 ) ) ;
#815=DIRECTION ( 'NONE',  ( 1.000000000000000000, 0.000000000000000000, 0.000000000000000000 ) ) ;
#826=ORIENTED_EDGE ( 'NONE', *, *, #5662, .F. ) ;
#837=ORIENTED_EDGE ( 'NONE', *, *, #4585, .F. ) ;
#842=DIRECTION ( 'NONE',  ( 0.000000000000000000, 0.000000000000000000, -1.000000000000000000 ) ) ;
#844=FACE_OUTER_BOUND ( 'NONE', #5680, .T. ) ;
#851=EDGE_LOOP ( 'NONE', ( #294, #2776 ) ) ;
#870=EDGE_LOOP ( 'NONE', ( #1828, #5276, #4459, #4079 ) ) ;
#874=ORIENTED_EDGE ( 'NONE', *, *, #4766, .F. ) ;
#877=VECTOR ( 'NONE', #4386, 1000.000000000000000 ) ;
#897=CIRCLE ( 'NONE', #250, 0.2500000000000002220 ) ;
#899=VERTEX_POINT ( 'NONE', #2864 ) ;
#902=DIRECTION ( 'NONE',  ( -0.000000000000000000, -0.000000000000000000, -1.000000000000000000 ) ) ;
#915=DIRECTION ( 'NONE',  ( -0.000000000000000000, -0.000000000000000000, -1.000000000000000000 ) ) ;
#916=EDGE_CURVE ( 'NONE', #1655, #5544, #2733, .T. ) ;
#923=( NAMED_UNIT ( * ) PLANE_ANGLE_UNIT ( ) SI_UNIT ( $, .RADIAN. ) );
#925=EDGE_CURVE ( 'NONE', #3736, #899, #5483, .T. ) ;
#927=DIRECTION ( 'NONE',  ( 0.000000000000000000, 0.000000000000000000, 1.000000000000000000 ) ) ;
#943=CARTESIAN_POINT ( 'NONE',  ( -25.00000000000000000, 0.000000000000000000, 8.000000000000000000 ) ) ;
#944=FACE_OUTER_BOUND ( 'NONE', #125, .T. ) ;
#945=LINE ( 'NONE', #3506, #3628 ) ;
#954=CARTESIAN_POINT ( 'NONE',  ( 17.55913978494622896, -14.85518798308249266, 8.000000000000000000 ) ) ;
#972=CIRCLE ( 'NONE', #3542, 5.000000000000000000 ) ;
#985=PLANE ( 'NONE',  #5010 ) ;
#986=ORIENTED_EDGE ( 'NONE', *, *, #1101, .T. ) ;
#990=AXIS2_PLACEMENT_3D ( 'NONE', #4490, #1470, #3658 ) ;
#993=VERTEX_POINT ( 'NONE', #5512 ) ;
#1000=VERTEX_POINT ( 'NONE', #3784 ) ;
#1007=DIRECTION ( 'NONE',  ( -1.000000000000000000, 0.000000000000000000, 0.000000000000000000 ) ) ;
#1010=DIRECTION ( 'NONE',  ( -0.000000000000000000, -0.000000000000000000, 1.000000000000000000 ) ) ;
#1018=ORIENTED_EDGE ( 'NONE', *, *, #395, .F. ) ;
#1036=ADVANCED_FACE ( 'NONE', ( #5139, #844 ), #1284, .T. ) ;
#1058=VECTOR ( 'NONE', #1938, 1000.000000000000000 ) ;
#1063=CIRCLE ( 'NONE', #1802, 25.00000000000000000 ) ;
#1064=DIRECTION ( 'NONE',  ( 1.000000000000000000, 0.000000000000000000, 0.000000000000000000 ) ) ;
#1069=CARTESIAN_POINT ( 'NONE',  ( -2.000000000000000000, 2.449293598294706414E-16, 4.000000000000000000 ) ) ;
#1101=EDGE_CURVE ( 'NONE', #2131, #3736, #3831, .T. ) ;
#1103=CARTESIAN_POINT ( 'NONE',  ( 0.000000000000000000, 0.000000000000000000, 2.000000000000000000 ) ) ;
#1125=CYLINDRICAL_SURFACE ( 'NONE', #4289, 2.000000000000000000 ) ;
#1132=EDGE_LOOP ( 'NONE', ( #2695, #837, #5190, #4747 ) ) ;
#1136=AXIS2_PLACEMENT_3D ( 'NONE', #2398, #707, #3382 ) ;
#1142=AXIS2_PLACEMENT_3D ( 'NONE', #5256, #2176, #2604 ) ;
#1166=ORIENTED_EDGE ( 'NONE', *, *, #2730, .F. ) ;
#1185=FACE_OUTER_BOUND ( 'NONE', #3674, .T. ) ;
#1191=EDGE_CURVE ( 'NONE', #4488, #1950, #3895, .T. ) ;
#1194=VERTEX_POINT ( 'NONE', #5650 ) ;
#1210=SURFACE_SIDE_STYLE ('',( #3450 ) ) ;
#1211=EDGE_CURVE ( 'NONE', #4096, #1000, #5227, .T. ) ;
#1239=CYLINDRICAL_SURFACE ( 'NONE', #3727, 25.00000000000000000 ) ;
#1242=FACE_OUTER_BOUND ( 'NONE', #3299, .T. ) ;
#1250=ADVANCED_FACE ( 'NONE', ( #2218 ), #1325, .F. ) ;
#1259=CIRCLE ( 'NONE', #3647, 2.000000000000000000 ) ;
#1265=VECTOR ( 'NONE', #4458, 1000.000000000000227 ) ;
#1268=( LENGTH_UNIT ( ) NAMED_UNIT ( * ) SI_UNIT ( .MILLI., .METRE. ) );
#1270=AXIS2_PLACEMENT_3D ( 'NONE', #1291, #3500, #3076 ) ;
#1278=EDGE_CURVE ( 'NONE', #1594, #4303, #1732, .T. ) ;
#1284=PLANE ( 'NONE',  #4206 ) ;
#1288=PLANE ( 'NONE',  #3078 ) ;
#1291=CARTESIAN_POINT ( 'NONE',  ( 0.000000000000000000, 0.000000000000000000, 4.000000000000000000 ) ) ;
#1298=LINE ( 'NONE', #455, #1880 ) ;
#1322=DIRECTION ( 'NONE',  ( -1.000000000000000000, 0.000000000000000000, 0.000000000000000000 ) ) ;
#1325=CYLINDRICAL_SURFACE ( 'NONE', #5398, 23.00000000000000000 ) ;
#1332=DIRECTION ( 'NONE',  ( -3.540989467475305966E-16, -1.000000000000000000, 0.000000000000000000 ) ) ;
#1336=AXIS2_PLACEMENT_3D ( 'NONE', #283, #2997, #5213 ) ;
#1346=CONICAL_SURFACE ( 'NONE', #4108, 2.000000000000000000, 1.029744258676656532 ) ;
#1366=CARTESIAN_POINT ( 'NONE',  ( 0.000000000000000000, 0.000000000000000000, 8.000000000000000000 ) ) ;
#1376=CARTESIAN_POINT ( 'NONE',  ( 25.00000000000000000, 3.061616997868383043E-15, 8.000000000000000000 ) ) ;
#1380=EDGE_CURVE ( 'NONE', #5397, #1594, #4393, .T. ) ;
#1386=CARTESIAN_POINT ( 'NONE',  ( 0.000000000000000000, 0.000000000000000000, 8.000000000000000000 ) ) ;
#1404=CARTESIAN_POINT ( 'NONE',  ( 23.00000000000000000, -2.168404344971008868E-16, -16.41957833606399930 ) ) ;
#1415=DIRECTION ( 'NONE',  ( -1.000000000000000000, 3.540989467475305966E-16, 0.000000000000000000 ) ) ;
#1420=AXIS2_PLACEMENT_3D ( 'NONE', #3872, #795, #4334 ) ;
#1421=EDGE_CURVE ( 'NONE', #993, #5595, #459, .T. ) ;
#1432=ORIENTED_EDGE ( 'NONE', *, *, #6, .T. ) ;
#1437=LINE ( 'NONE', #1464, #2063 ) ;
#1441=LINE ( 'NONE', #5325, #4078 ) ;
#1453=AXIS2_PLACEMENT_3D ( 'NONE', #5634, #2932, #2038 ) ;
#1454=EDGE_CURVE ( 'NONE', #1655, #30, #4000, .T. ) ;
#1457=ORIENTED_EDGE ( 'NONE', *, *, #5077, .F. ) ;
#1464=CARTESIAN_POINT ( 'NONE',  ( -2.000000000000000000, 2.449293598294706414E-16, 4.000000000000000000 ) ) ;
#1470=DIRECTION ( 'NONE',  ( 0.000000000000000000, 0.000000000000000000, 1.000000000000000000 ) ) ;
#1474=DIRECTION ( 'NONE',  ( 1.000000000000000000, 0.000000000000000000, 0.000000000000000000 ) ) ;
#1491=DIRECTION ( 'NONE',  ( 0.000000000000000000, 0.000000000000000000, -1.000000000000000000 ) ) ;
#1510=EDGE_CURVE ( 'NONE', #1733, #4303, #3681, .T. ) ;
#1516=ADVANCED_FACE ( 'NONE', ( #2325 ), #2921, .F. ) ;
#1520=VECTOR ( 'NONE', #1332, 1000.000000000000000 ) ;
#1521=ORIENTED_EDGE ( 'NONE', *, *, #4924, .F. ) ;
#1524=EDGE_CURVE ( 'NONE', #5544, #2880, #4972, .T. ) ;
#1533=CARTESIAN_POINT ( 'NONE',  ( 0.000000000000000000, 0.000000000000000000, 8.000000000000000000 ) ) ;
#1542=CARTESIAN_POINT ( 'NONE',  ( -25.00000000000000000, 0.000000000000000000, 8.000000000000000000 ) ) ;
#1560=ADVANCED_FACE ( 'NONE', ( #4058 ), #5467, .T. ) ;
#1561=PLANE ( 'NONE',  #3730 ) ;
#1569=DIRECTION ( 'NONE',  ( 0.000000000000000000, 0.000000000000000000, 1.000000000000000000 ) ) ;
#1584=FILL_AREA_STYLE_COLOUR ( '', #3537 ) ;
#1594=VERTEX_POINT ( 'NONE', #3626 ) ;
#1595=DIRECTION ( 'NONE',  ( 1.000000000000000000, 0.000000000000000000, 0.000000000000000000 ) ) ;
#1597=ADVANCED_FACE ( 'NONE', ( #2851, #4174 ), #2413, .T. ) ;
#1614=DIRECTION ( 'NONE',  ( 0.000000000000000000, 0.000000000000000000, 1.000000000000000000 ) ) ;
#1617=AXIS2_PLACEMENT_3D ( 'NONE', #2277, #1415, #3176 ) ;
#1618=CYLINDRICAL_SURFACE ( 'NONE', #2817, 0.2500000000000002220 ) ;
#1628=CARTESIAN_POINT ( 'NONE',  ( -5.000000000000000000, 4.999999999999978684, 8.000000000000000000 ) ) ;
#1636=EDGE_CURVE ( 'NONE', #2131, #5617, #897, .T. ) ;
#1641=CYLINDRICAL_SURFACE ( 'NONE', #3656, 0.2500000000000002220 ) ;
#1655=VERTEX_POINT ( 'NONE', #4518 ) ;
#1656=DIRECTION ( 'NONE',  ( -1.000000000000000000, 0.000000000000000000, 0.000000000000000000 ) ) ;
#1660=ORIENTED_EDGE ( 'NONE', *, *, #4578, .F. ) ;
#1668=SHAPE_REPRESENTATION_RELATIONSHIP ( 'NONE' , 'NONE' ,  #3487, #69 ) ;
#1673=DIRECTION ( 'NONE',  ( -0.000000000000000000, -0.000000000000000000, -1.000000000000000000 ) ) ;
#1683=DIRECTION ( 'NONE',  ( -1.000000000000000000, 0.000000000000000000, 0.000000000000000000 ) ) ;
#1698=CARTESIAN_POINT ( 'NONE',  ( 17.99999999999999289, -17.34935157289748631, 4.000000000000000000 ) ) ;
#1708=EDGE_LOOP ( 'NONE', ( #4955, #2629, #2200, #4897 ) ) ;
#1716=EDGE_CURVE ( 'NONE', #5397, #5155, #4144, .T. ) ;
#1720=CIRCLE ( 'NONE', #2081, 5.000000000000000000 ) ;
#1723=VECTOR ( 'NONE', #4700, 1000.000000000000000 ) ;
#1732=LINE ( 'NONE', #2191, #1910 ) ;
#1733=VERTEX_POINT ( 'NONE', #4659 ) ;
#1739=CARTESIAN_POINT ( 'NONE',  ( -5.000000000000000000, 4.999999999999978684, 5.000000000000000000 ) ) ;
#1762=ORIENTED_EDGE ( 'NONE', *, *, #4513, .T. ) ;
#1768=ADVANCED_FACE ( 'NONE', ( #4318 ), #1641, .T. ) ;
#1782=CARTESIAN_POINT ( 'NONE',  ( 0.000000000000000000, 0.000000000000000000, 8.000000000000000000 ) ) ;
#1783=ORIENTED_EDGE ( 'NONE', *, *, #5268, .T. ) ;
#1788=DIRECTION ( 'NONE',  ( 0.000000000000000000, 0.000000000000000000, 1.000000000000000000 ) ) ;
#1802=AXIS2_PLACEMENT_3D ( 'NONE', #5128, #1614, #5585 ) ;
#1814=DIRECTION ( 'NONE',  ( -0.000000000000000000, -0.000000000000000000, -1.000000000000000000 ) ) ;
#1818=VECTOR ( 'NONE', #5687, 1000.000000000000000 ) ;
#1822=ORIENTED_EDGE ( 'NONE', *, *, #3881, .T. ) ;
#1828=ORIENTED_EDGE ( 'NONE', *, *, #1211, .F. ) ;
#1835=EDGE_LOOP ( 'NONE', ( #1457, #2411, #1848 ) ) ;
#1843=DIRECTION ( 'NONE',  ( 1.000000000000000000, 0.000000000000000000, 0.000000000000000000 ) ) ;
#1848=ORIENTED_EDGE ( 'NONE', *, *, #81, .T. ) ;
#1864=EDGE_CURVE ( 'NONE', #525, #1594, #2993, .T. ) ;
#1872=EDGE_CURVE ( 'NONE', #5155, #4844, #3934, .T. ) ;
#1880=VECTOR ( 'NONE', #4426, 1000.000000000000000 ) ;
#1907=CARTESIAN_POINT ( 'NONE',  ( 0.000000000000000000, 0.000000000000000000, 8.000000000000000000 ) ) ;
#1910=VECTOR ( 'NONE', #2243, 1000.000000000000000 ) ;
#1927=EDGE_CURVE ( 'NONE', #3499, #4270, #5628, .T. ) ;
#1938=DIRECTION ( 'NONE',  ( 0.000000000000000000, 0.000000000000000000, 1.000000000000000000 ) ) ;
#1950=VERTEX_POINT ( 'NONE', #19 ) ;
#1952=CARTESIAN_POINT ( 'NONE',  ( 23.00000000000000000, -2.168404344971008868E-16, 8.000000000000000000 ) ) ;
#1959=FACE_OUTER_BOUND ( 'NONE', #3118, .T. ) ;
#1968=ORIENTED_EDGE ( 'NONE', *, *, #1510, .F. ) ;
#1970=CIRCLE ( 'NONE', #4719, 2.000000000000000000 ) ;
#1973=EDGE_CURVE ( 'NONE', #2459, #2880, #5495, .T. ) ;
#1985=DIRECTION ( 'NONE',  ( 1.000000000000000000, 0.000000000000000000, 0.000000000000000000 ) ) ;
#1990=CARTESIAN_POINT ( 'NONE',  ( 0.000000000000000000, 0.000000000000000000, 8.000000000000000000 ) ) ;
#1992=DIRECTION ( 'NONE',  ( 1.000000000000000000, 0.000000000000000000, 0.000000000000000000 ) ) ;
#2004=DIRECTION ( 'NONE',  ( 0.000000000000000000, 0.000000000000000000, 1.000000000000000000 ) ) ;
#2011=CARTESIAN_POINT ( 'NONE',  ( 23.00000000000000000, -2.168404344971008868E-16, 8.000000000000000000 ) ) ;
#2019=CARTESIAN_POINT ( 'NONE',  ( 0.000000000000000000, 0.000000000000000000, 8.000000000000000000 ) ) ;
#2025=CARTESIAN_POINT ( 'NONE',  ( 4.999999999999914735, 24.49489742783179835, 8.000000000000000000 ) ) ;
#2038=DIRECTION ( 'NONE',  ( 1.000000000000000000, 0.000000000000000000, 0.000000000000000000 ) ) ;
#2040=PRODUCT_DEFINITION ( 'UNKNOWN', '', #2144, #384 ) ;
#2042=CARTESIAN_POINT ( 'NONE',  ( 2.000000000000000000, 0.000000000000000000, 8.000000000000000000 ) ) ;
#2052=ORIENTED_EDGE ( 'NONE', *, *, #4011, .T. ) ;
#2053=CARTESIAN_POINT ( 'NONE',  ( 0.000000000000000000, 0.000000000000000000, 4.000000000000000000 ) ) ;
#2063=VECTOR ( 'NONE', #4115, 1000.000000000000227 ) ;
#2074=FACE_OUTER_BOUND ( 'NONE', #1835, .T. ) ;
#2081=AXIS2_PLACEMENT_3D ( 'NONE', #4491, #4892, #1843 ) ;
#2092=ORIENTED_EDGE ( 'NONE', *, *, #1927, .F. ) ;
#2094=DIRECTION ( 'NONE',  ( -1.000000000000000000, 0.000000000000000000, 0.000000000000000000 ) ) ;
#2096=CARTESIAN_POINT ( 'NONE',  ( 4.999999999999923617, 22.44994432064366308, 8.000000000000000000 ) ) ;
#2100=CARTESIAN_POINT ( 'NONE',  ( -2.000000000000000000, 2.449293598294706414E-16, 8.000000000000000000 ) ) ;
#2104=CYLINDRICAL_SURFACE ( 'NONE', #4741, 5.000000000000000000 ) ;
#2108=ORIENTED_EDGE ( 'NONE', *, *, #3321, .T. ) ;
#2129=DIRECTION ( 'NONE',  ( 1.000000000000000000, 0.000000000000000000, 0.000000000000000000 ) ) ;
#2131=VERTEX_POINT ( 'NONE', #3270 ) ;
#2133=CARTESIAN_POINT ( 'NONE',  ( -5.000000000000000000, 0.000000000000000000, 8.000000000000000000 ) ) ;
#2144=PRODUCT_DEFINITION_FORMATION_WITH_SPECIFIED_SOURCE ( 'ANY', '', #5145, .NOT_KNOWN. ) ;
#2145=DIRECTION ( 'NONE',  ( 0.000000000000000000, 0.000000000000000000, -1.000000000000000000 ) ) ;
#2147=ORIENTED_EDGE ( 'NONE', *, *, #4585, .T. ) ;
#2156=CIRCLE ( 'NONE', #588, 23.00000000000000000 ) ;
#2157=CARTESIAN_POINT ( 'NONE',  ( 5.000000000000000000, 5.000000000000022204, 5.000000000000000000 ) ) ;
#2162=ORIENTED_EDGE ( 'NONE', *, *, #395, .T. ) ;
#2167=VECTOR ( 'NONE', #2531, 1000.000000000000000 ) ;
#2176=DIRECTION ( 'NONE',  ( 0.000000000000000000, 0.000000000000000000, 1.000000000000000000 ) ) ;
#2191=CARTESIAN_POINT ( 'NONE',  ( 5.000000000000000000, 5.000000000000022204, 8.000000000000000000 ) ) ;
#2195=ADVANCED_FACE ( 'NONE', ( #669 ), #2420, .T. ) ;
#2200=ORIENTED_EDGE ( 'NONE', *, *, #2956, .F. ) ;
#2201=ORIENTED_EDGE ( 'NONE', *, *, #5546, .F. ) ;
#2214=CARTESIAN_POINT ( 'NONE',  ( 17.99999999999999289, -15.01665741768121443, 8.000000000000000000 ) ) ;
#2218=FACE_OUTER_BOUND ( 'NONE', #2738, .T. ) ;
#2243=DIRECTION ( 'NONE',  ( -4.364351673553916694E-15, 1.000000000000000000, 0.000000000000000000 ) ) ;
#2250=EDGE_LOOP ( 'NONE', ( #2639, #4690, #2162 ) ) ;
#2258=VERTEX_POINT ( 'NONE', #2831 ) ;
#2276=FACE_OUTER_BOUND ( 'NONE', #2747, .T. ) ;
#2277=CARTESIAN_POINT ( 'NONE',  ( 18.00000000000000000, 1.553654299240552096E-15, -16.41957833606399930 ) ) ;
#2303=DIRECTION ( 'NONE',  ( 1.000000000000000000, 0.000000000000000000, 0.000000000000000000 ) ) ;
#2305=ORIENTED_EDGE ( 'NONE', *, *, #1524, .F. ) ;
#2307=ORIENTED_EDGE ( 'NONE', *, *, #5183, .F. ) ;
#2325=FACE_OUTER_BOUND ( 'NONE', #2250, .T. ) ;
#2338=( GEOMETRIC_REPRESENTATION_CONTEXT ( 3 ) GLOBAL_UNCERTAINTY_ASSIGNED_CONTEXT ( ( #3315 ) ) GLOBAL_UNIT_ASSIGNED_CONTEXT ( ( #5388, #4520, #3660 ) ) REPRESENTATION_CONTEXT ( 'NONE', 'WORKASPACE' ) );
#2340=CARTESIAN_POINT ( 'NONE',  ( 17.99999999999999289, -17.34935157289748631, 8.000000000000000000 ) ) ;
#2346=AXIS2_PLACEMENT_3D ( 'NONE', #1990, #3744, #5097 ) ;
#2363=DIRECTION ( 'NONE',  ( 1.000000000000000000, 0.000000000000000000, 0.000000000000000000 ) ) ;
#2388=DIRECTION ( 'NONE',  ( -0.000000000000000000, -0.000000000000000000, -1.000000000000000000 ) ) ;
#2398=CARTESIAN_POINT ( 'NONE',  ( 0.000000000000000000, 0.000000000000000000, 5.000000000000000000 ) ) ;
#2411=ORIENTED_EDGE ( 'NONE', *, *, #1421, .T. ) ;
#2413=PLANE ( 'NONE',  #4479 ) ;
#2420=CYLINDRICAL_SURFACE ( 'NONE', #2900, 5.000000000000000000 ) ;
#2426=PRODUCT_DEFINITION_SHAPE ( 'NONE', 'NONE',  #2040 ) ;
#2441=CIRCLE ( 'NONE', #4097, 23.00000000000000000 ) ;
#2448=CARTESIAN_POINT ( 'NONE',  ( 2.000000000000000000, 0.000000000000000000, 4.000000000000000000 ) ) ;
#2455=ADVANCED_FACE ( 'NONE', ( #1242 ), #3004, .T. ) ;
#2458=PLANE ( 'NONE',  #1136 ) ;
#2459=VERTEX_POINT ( 'NONE', #3862 ) ;
#2461=VERTEX_POINT ( 'NONE', #2133 ) ;
#2476=PRESENTATION_STYLE_ASSIGNMENT (( #4742 ) ) ;
#2489=DIRECTION ( 'NONE',  ( 1.000000000000000000, 0.000000000000000000, -0.000000000000000000 ) ) ;
#2503=CARTESIAN_POINT ( 'NONE',  ( 0.000000000000000000, 0.000000000000000000, 4.000000000000000000 ) ) ;
#2520=CARTESIAN_POINT ( 'NONE',  ( 0.000000000000000000, 0.000000000000000000, 8.000000000000000000 ) ) ;
#2524=MECHANICAL_DESIGN_GEOMETRIC_PRESENTATION_REPRESENTATION('',(#5004),#4279);
#2527=VECTOR ( 'NONE', #3463, 1000.000000000000000 ) ;
#2531=DIRECTION ( 'NONE',  ( -0.000000000000000000, -0.000000000000000000, 1.000000000000000000 ) ) ;
#2532=ORIENTED_EDGE ( 'NONE', *, *, #1973, .T. ) ;
#2551=ORIENTED_EDGE ( 'NONE', *, *, #925, .F. ) ;
#2557=EDGE_CURVE ( 'NONE', #2855, #2946, #4860, .T. ) ;
#2567=EDGE_CURVE ( 'NONE', #4270, #2946, #2714, .T. ) ;
#2604=DIRECTION ( 'NONE',  ( 1.000000000000000000, 0.000000000000000000, 0.000000000000000000 ) ) ;
#2617=CARTESIAN_POINT ( 'NONE',  ( 23.48484848484848442, -8.570991287109677614, 8.000000000000000000 ) ) ;
#2624=DIRECTION ( 'NONE',  ( 1.000000000000000000, 0.000000000000000000, 0.000000000000000000 ) ) ;
#2629=ORIENTED_EDGE ( 'NONE', *, *, #1191, .F. ) ;
#2632=EDGE_CURVE ( 'NONE', #2855, #899, #2805, .T. ) ;
#2639=ORIENTED_EDGE ( 'NONE', *, *, #1421, .F. ) ;
#2648=VECTOR ( 'NONE', #1814, 1000.000000000000000 ) ;
#2673=DIRECTION ( 'NONE',  ( 1.000000000000000000, 0.000000000000000000, 0.000000000000000000 ) ) ;
#2678=ORIENTED_EDGE ( 'NONE', *, *, #1973, .F. ) ;
#2683=ORIENTED_EDGE ( 'NONE', *, *, #3291, .F. ) ;
#2688=ORIENTED_EDGE ( 'NONE', *, *, #2632, .T. ) ;
#2693=PRODUCT_CONTEXT ( 'NONE', #5525, 'mechanical' ) ;
#2695=ORIENTED_EDGE ( 'NONE', *, *, #1636, .F. ) ;
#2702=CARTESIAN_POINT ( 'NONE',  ( 0.000000000000000000, 0.000000000000000000, 8.000000000000000000 ) ) ;
#2704=AXIS2_PLACEMENT_3D ( 'NONE', #3932, #2145, #1683 ) ;
#2708=UNCERTAINTY_MEASURE_WITH_UNIT (LENGTH_MEASURE( 1.000000000000000082E-05 ), #5247, 'distance_accuracy_value', 'NONE');
#2711=DIRECTION ( 'NONE',  ( 0.000000000000000000, 0.000000000000000000, 1.000000000000000000 ) ) ;
#2714=CIRCLE ( 'NONE', #134, 25.00000000000000000 ) ;
#2730=EDGE_CURVE ( 'NONE', #5595, #132, #779, .T. ) ;
#2733=CIRCLE ( 'NONE', #5304, 23.00000000000000000 ) ;
#2734=CARTESIAN_POINT ( 'NONE',  ( 22.99999999999999645, -8.485281374238580199, 8.000000000000000000 ) ) ;
#2737=ADVANCED_FACE ( 'NONE', ( #3799 ), #1239, .T. ) ;
#2738=EDGE_LOOP ( 'NONE', ( #4379, #5404, #5162, #3648, #1521, #411, #3808, #4125, #1660 ) ) ;
#2744=CARTESIAN_POINT ( 'NONE',  ( 0.000000000000000000, 0.000000000000000000, 2.000000000000000000 ) ) ;
#2745=CARTESIAN_POINT ( 'NONE',  ( 17.99999999999999289, -15.01665741768121443, 4.000000000000000000 ) ) ;
#2747=EDGE_LOOP ( 'NONE', ( #3352, #3950, #4438, #4650, #4225, #315 ) ) ;
#2761=LINE ( 'NONE', #2815, #5000 ) ;
#2776=ORIENTED_EDGE ( 'NONE', *, *, #4513, .F. ) ;
#2805=CIRCLE ( 'NONE', #5003, 25.00000000000000000 ) ;
#2806=CARTESIAN_POINT ( 'NONE',  ( 17.55913978494622896, -14.85518798308249266, 4.000000000000000000 ) ) ;
#2815=CARTESIAN_POINT ( 'NONE',  ( 18.00000000000000000, 1.553654299240552096E-15, 4.000000000000000000 ) ) ;
#2817=AXIS2_PLACEMENT_3D ( 'NONE', #3801, #5219, #3861 ) ;
#2820=ORIENTED_EDGE ( 'NONE', *, *, #3291, .T. ) ;
#2831=CARTESIAN_POINT ( 'NONE',  ( 5.000000000000000000, 6.123233995736766282E-16, 8.000000000000000000 ) ) ;
#2849=ORIENTED_EDGE ( 'NONE', *, *, #1636, .T. ) ;
#2851=FACE_BOUND ( 'NONE', #851, .T. ) ;
#2855=VERTEX_POINT ( 'NONE', #1542 ) ;
#2856=DIRECTION ( 'NONE',  ( -0.000000000000000000, -0.000000000000000000, 1.000000000000000000 ) ) ;
#2864=CARTESIAN_POINT ( 'NONE',  ( 17.99999999999999289, -17.34935157289748631, 8.000000000000000000 ) ) ;
#2878=CARTESIAN_POINT ( 'NONE',  ( 23.00000000000000000, -2.168404344971008868E-16, -16.41957833606399930 ) ) ;
#2880=VERTEX_POINT ( 'NONE', #2806 ) ;
#2884=CIRCLE ( 'NONE', #4353, 5.000000000000000000 ) ;
#2887=ORIENTED_EDGE ( 'NONE', *, *, #3014, .F. ) ;
#2889=DIRECTION ( 'NONE',  ( 1.000000000000000000, 0.000000000000000000, 0.000000000000000000 ) ) ;
#2900=AXIS2_PLACEMENT_3D ( 'NONE', #1533, #3713, #5132 ) ;
#2921=CONICAL_SURFACE ( 'NONE', #4119, 2.000000000000000000, 1.029744258676656532 ) ;
#2926=ORIENTED_EDGE ( 'NONE', *, *, #4980, .F. ) ;
#2928=EDGE_CURVE ( 'NONE', #30, #3011, #2441, .T. ) ;
#2932=DIRECTION ( 'NONE',  ( 0.000000000000000000, 0.000000000000000000, 1.000000000000000000 ) ) ;
#2934=( NAMED_UNIT ( * ) PLANE_ANGLE_UNIT ( ) SI_UNIT ( $, .RADIAN. ) );
#2946=VERTEX_POINT ( 'NONE', #4590 ) ;
#2956=EDGE_CURVE ( 'NONE', #4096, #4488, #674, .T. ) ;
#2966=CARTESIAN_POINT ( 'NONE',  ( 0.000000000000000000, 0.000000000000000000, 4.000000000000000000 ) ) ;
#2982=CARTESIAN_POINT ( 'NONE',  ( 5.000000000000000000, 6.123233995736766282E-16, 2.000000000000000000 ) ) ;
#2988=CARTESIAN_POINT ( 'NONE',  ( 5.000000000000000000, 6.123233995736766282E-16, 8.000000000000000000 ) ) ;
#2993=LINE ( 'NONE', #2096, #4298 ) ;
#2997=DIRECTION ( 'NONE',  ( 0.000000000000000000, 0.000000000000000000, 1.000000000000000000 ) ) ;
#3004=PLANE ( 'NONE',  #4729 ) ;
#3011=VERTEX_POINT ( 'NONE', #4242 ) ;
#3014=EDGE_CURVE ( 'NONE', #3426, #4851, #293, .T. ) ;
#3016=VECTOR ( 'NONE', #3387, 1000.000000000000000 ) ;
#3022=EDGE_CURVE ( 'NONE', #1000, #1950, #5225, .T. ) ;
#3028=DIRECTION ( 'NONE',  ( 1.000000000000000000, 4.364351673553916694E-15, 0.000000000000000000 ) ) ;
#3043=CARTESIAN_POINT ( 'NONE',  ( -5.000000000000000000, 4.999999999999978684, 5.000000000000000000 ) ) ;
#3054=DIRECTION ( 'NONE',  ( -4.364351673553916694E-15, 1.000000000000000000, 0.000000000000000000 ) ) ;
#3071=EDGE_CURVE ( 'NONE', #2880, #3426, #50, .T. ) ;
#3074=EDGE_LOOP ( 'NONE', ( #4007, #165, #2052, #5138 ) ) ;
#3076=DIRECTION ( 'NONE',  ( -1.000000000000000000, 0.000000000000000000, 0.000000000000000000 ) ) ;
#3078=AXIS2_PLACEMENT_3D ( 'NONE', #3043, #5684, #3497 ) ;
#3093=EDGE_LOOP ( 'NONE', ( #2092, #3492, #2147, #986, #5188, #5271, #4188, #150 ) ) ;
#3096=LINE ( 'NONE', #3581, #710 ) ;
#3118=EDGE_LOOP ( 'NONE', ( #471, #5038, #372, #5083 ) ) ;
#3139=PLANE ( 'NONE',  #4539 ) ;
#3150=EDGE_LOOP ( 'NONE', ( #874, #493 ) ) ;
#3176=DIRECTION ( 'NONE',  ( -3.540989467475305966E-16, -1.000000000000000000, 0.000000000000000000 ) ) ;
#3208=CARTESIAN_POINT ( 'NONE',  ( 0.000000000000000000, 0.000000000000000000, 4.000000000000000000 ) ) ;
#3227=EDGE_CURVE ( 'NONE', #3499, #4303, #4549, .T. ) ;
#3229=CARTESIAN_POINT ( 'NONE',  ( 0.000000000000000000, 0.000000000000000000, 4.000000000000000000 ) ) ;
#3256=DIRECTION ( 'NONE',  ( 0.000000000000000000, 0.000000000000000000, 1.000000000000000000 ) ) ;
#3268=ORIENTED_EDGE ( 'NONE', *, *, #3464, .F. ) ;
#3270=CARTESIAN_POINT ( 'NONE',  ( 23.48484848484848442, -8.570991287109677614, 4.000000000000000000 ) ) ;
#3277=CLOSED_SHELL ( 'NONE', ( #1516, #251, #481, #3856, #2737, #1560, #5463, #4484, #3330, #1250, #1036, #2195, #1597, #196, #3779, #3423, #2455, #3619, #4843, #4825, #4194, #306, #1768 ) ) ;
#3284=DIRECTION ( 'NONE',  ( -0.000000000000000000, -0.000000000000000000, 1.000000000000000000 ) ) ;
#3291=EDGE_CURVE ( 'NONE', #2258, #2461, #972, .T. ) ;
#3299=EDGE_LOOP ( 'NONE', ( #5565, #241, #4404, #2201 ) ) ;
#3300=CARTESIAN_POINT ( 'NONE',  ( 0.000000000000000000, 0.000000000000000000, 8.000000000000000000 ) ) ;
#3315=UNCERTAINTY_MEASURE_WITH_UNIT (LENGTH_MEASURE( 1.000000000000000082E-05 ), #5388, 'distance_accuracy_value', 'NONE');
#3321=EDGE_CURVE ( 'NONE', #4851, #899, #577, .T. ) ;
#3330=ADVANCED_FACE ( 'NONE', ( #5277 ), #985, .F. ) ;
#3335=LINE ( 'NONE', #2988, #4368 ) ;
#3338=ORIENTED_EDGE ( 'NONE', *, *, #3071, .F. ) ;
#3346=DIRECTION ( 'NONE',  ( 1.000000000000000000, 0.000000000000000000, 0.000000000000000000 ) ) ;
#3352=ORIENTED_EDGE ( 'NONE', *, *, #1716, .T. ) ;
#3356=AXIS2_PLACEMENT_3D ( 'NONE', #2520, #4284, #2094 ) ;
#3373=( GEOMETRIC_REPRESENTATION_CONTEXT ( 3 ) GLOBAL_UNCERTAINTY_ASSIGNED_CONTEXT ( ( #2708 ) ) GLOBAL_UNIT_ASSIGNED_CONTEXT ( ( #5247, #923, #4432 ) ) REPRESENTATION_CONTEXT ( 'NONE', 'WORKASPACE' ) );
#3376=ORIENTED_EDGE ( 'NONE', *, *, #624, .T. ) ;
#3382=DIRECTION ( 'NONE',  ( -1.000000000000000000, 0.000000000000000000, -0.000000000000000000 ) ) ;
#3386=VECTOR ( 'NONE', #5061, 1000.000000000000000 ) ;
#3387=DIRECTION ( 'NONE',  ( -4.364351673553916694E-15, 1.000000000000000000, 0.000000000000000000 ) ) ;
#3409=CARTESIAN_POINT ( 'NONE',  ( 17.74999999999999289, -15.01665741768121443, 4.000000000000000000 ) ) ;
#3423=ADVANCED_FACE ( 'NONE', ( #4465 ), #524, .F. ) ;
#3425=DIRECTION ( 'NONE',  ( -0.000000000000000000, -0.000000000000000000, 1.000000000000000000 ) ) ;
#3426=VERTEX_POINT ( 'NONE', #2745 ) ;
#3450=SURFACE_STYLE_FILL_AREA ( #746 ) ;
#3454=ORIENTED_EDGE ( 'NONE', *, *, #3022, .F. ) ;
#3457=DIRECTION ( 'NONE',  ( -1.000000000000000000, 3.540989467475305966E-16, 0.000000000000000000 ) ) ;
#3463=DIRECTION ( 'NONE',  ( 0.000000000000000000, 0.000000000000000000, 1.000000000000000000 ) ) ;
#3464=EDGE_CURVE ( 'NONE', #4488, #1655, #4198, .T. ) ;
#3481=LINE ( 'NONE', #2100, #4553 ) ;
#3482=DIRECTION ( 'NONE',  ( 0.000000000000000000, 0.000000000000000000, 1.000000000000000000 ) ) ;
#3487=SHAPE_REPRESENTATION ( 'outer cover 1', ( #1336 ), #2338 ) ;
#3492=ORIENTED_EDGE ( 'NONE', *, *, #4154, .F. ) ;
#3497=DIRECTION ( 'NONE',  ( -4.364351673553916694E-15, 1.000000000000000000, 0.000000000000000000 ) ) ;
#3499=VERTEX_POINT ( 'NONE', #4580 ) ;
#3500=DIRECTION ( 'NONE',  ( 0.000000000000000000, 0.000000000000000000, -1.000000000000000000 ) ) ;
#3506=CARTESIAN_POINT ( 'NONE',  ( 23.00000000000000000, -2.168404344971008868E-16, 4.000000000000000000 ) ) ;
#3537=COLOUR_RGB ( '',0.8941176470588234615, 0.8941176470588234615, 0.8941176470588234615 ) ;
#3542=AXIS2_PLACEMENT_3D ( 'NONE', #3603, #5358, #4522 ) ;
#3573=ORIENTED_EDGE ( 'NONE', *, *, #2928, .T. ) ;
#3581=CARTESIAN_POINT ( 'NONE',  ( 23.00000000000000000, 2.816687638038912352E-15, 8.000000000000000000 ) ) ;
#3603=CARTESIAN_POINT ( 'NONE',  ( 0.000000000000000000, 0.000000000000000000, 8.000000000000000000 ) ) ;
#3619=ADVANCED_FACE ( 'NONE', ( #4095 ), #1561, .F. ) ;
#3625=CIRCLE ( 'NONE', #1420, 25.00000000000000000 ) ;
#3626=CARTESIAN_POINT ( 'NONE',  ( 4.999999999999923617, 22.44994432064366308, 8.000000000000000000 ) ) ;
#3628=VECTOR ( 'NONE', #5667, 1000.000000000000000 ) ;
#3629=CARTESIAN_POINT ( 'NONE',  ( 22.99999999999999645, -8.485281374238580199, 4.000000000000000000 ) ) ;
#3630=DIRECTION ( 'NONE',  ( 1.000000000000000000, 0.000000000000000000, 0.000000000000000000 ) ) ;
#3647=AXIS2_PLACEMENT_3D ( 'NONE', #4636, #5418, #205 ) ;
#3648=ORIENTED_EDGE ( 'NONE', *, *, #1864, .F. ) ;
#3655=EDGE_LOOP ( 'NONE', ( #2683, #1783, #711, #5573 ) ) ;
#3656=AXIS2_PLACEMENT_3D ( 'NONE', #367, #4684, #744 ) ;
#3658=DIRECTION ( 'NONE',  ( 1.000000000000000000, 0.000000000000000000, -0.000000000000000000 ) ) ;
#3660=( NAMED_UNIT ( * ) SI_UNIT ( $, .STERADIAN. ) SOLID_ANGLE_UNIT ( ) );
#3669=ORIENTED_EDGE ( 'NONE', *, *, #1191, .T. ) ;
#3674=EDGE_LOOP ( 'NONE', ( #2678, #1432, #5089, #5071, #356, #4537 ) ) ;
#3679=EDGE_LOOP ( 'NONE', ( #4753, #4791 ) ) ;
#3681=LINE ( 'NONE', #569, #3386 ) ;
#3694=DIRECTION ( 'NONE',  ( 0.000000000000000000, 0.000000000000000000, 1.000000000000000000 ) ) ;
#3705=DIRECTION ( 'NONE',  ( -3.540989467475305966E-16, -1.000000000000000000, 0.000000000000000000 ) ) ;
#3711=EDGE_LOOP ( 'NONE', ( #2307, #4927, #2108, #2551 ) ) ;
#3713=DIRECTION ( 'NONE',  ( -0.000000000000000000, -0.000000000000000000, -1.000000000000000000 ) ) ;
#3727=AXIS2_PLACEMENT_3D ( 'NONE', #2019, #3773, #4294 ) ;
#3730=AXIS2_PLACEMENT_3D ( 'NONE', #3229, #148, #4180 ) ;
#3736=VERTEX_POINT ( 'NONE', #1698 ) ;
#3744=DIRECTION ( 'NONE',  ( 0.000000000000000000, 0.000000000000000000, 1.000000000000000000 ) ) ;
#3771=UNCERTAINTY_MEASURE_WITH_UNIT (LENGTH_MEASURE( 1.000000000000000082E-05 ), #1268, 'distance_accuracy_value', 'NONE');
#3773=DIRECTION ( 'NONE',  ( -0.000000000000000000, -0.000000000000000000, -1.000000000000000000 ) ) ;
#3775=DIRECTION ( 'NONE',  ( -0.000000000000000000, -0.000000000000000000, 1.000000000000000000 ) ) ;
#3779=ADVANCED_FACE ( 'NONE', ( #2074 ), #1346, .F. ) ;
#3784=CARTESIAN_POINT ( 'NONE',  ( -5.000000000000085265, 24.49489742783176638, 5.000000000000000000 ) ) ;
#3799=FACE_OUTER_BOUND ( 'NONE', #4366, .T. ) ;
#3801=CARTESIAN_POINT ( 'NONE',  ( 23.24999999999999645, -8.485281374238580199, 8.000000000000000000 ) ) ;
#3808=ORIENTED_EDGE ( 'NONE', *, *, #3464, .T. ) ;
#3814=EDGE_CURVE ( 'NONE', #92, #1194, #3481, .T. ) ;
#3831=CIRCLE ( 'NONE', #4563, 25.00000000000000000 ) ;
#3837=VECTOR ( 'NONE', #3705, 1000.000000000000000 ) ;
#3856=ADVANCED_FACE ( 'NONE', ( #1185 ), #4745, .F. ) ;
#3859=CARTESIAN_POINT ( 'NONE',  ( 0.000000000000000000, 0.000000000000000000, 8.000000000000000000 ) ) ;
#3861=DIRECTION ( 'NONE',  ( -1.000000000000000000, 0.000000000000000000, 0.000000000000000000 ) ) ;
#3862=CARTESIAN_POINT ( 'NONE',  ( 23.00000000000000000, -8.144275775193202933E-15, 4.000000000000000000 ) ) ;
#3872=CARTESIAN_POINT ( 'NONE',  ( 0.000000000000000000, 0.000000000000000000, 0.000000000000000000 ) ) ;
#3881=EDGE_CURVE ( 'NONE', #1950, #2855, #1063, .T. ) ;
#3886=DIRECTION ( 'NONE',  ( 0.000000000000000000, 0.000000000000000000, 1.000000000000000000 ) ) ;
#3895=LINE ( 'NONE', #1628, #3016 ) ;
#3901=CIRCLE ( 'NONE', #4081, 23.00000000000000000 ) ;
#3914=DIRECTION ( 'NONE',  ( 0.000000000000000000, 0.000000000000000000, 1.000000000000000000 ) ) ;
#3920=CIRCLE ( 'NONE', #5643, 2.000000000000000000 ) ;
#3922=MECHANICAL_DESIGN_GEOMETRIC_PRESENTATION_REPRESENTATION('',(#4931),#3373);
#3932=CARTESIAN_POINT ( 'NONE',  ( 0.000000000000000000, 0.000000000000000000, 5.000000000000000000 ) ) ;
#3934=CIRCLE ( 'NONE', #1453, 0.2500000000000002220 ) ;
#3950=ORIENTED_EDGE ( 'NONE', *, *, #1872, .T. ) ;
#3951=DIRECTION ( 'NONE',  ( 1.000000000000000000, 0.000000000000000000, 0.000000000000000000 ) ) ;
#3969=DIRECTION ( 'NONE',  ( -0.000000000000000000, -0.000000000000000000, -1.000000000000000000 ) ) ;
#4000=LINE ( 'NONE', #57, #2648 ) ;
#4003=AXIS2_PLACEMENT_3D ( 'NONE', #1366, #1788, #3951 ) ;
#4007=ORIENTED_EDGE ( 'NONE', *, *, #5268, .F. ) ;
#4011=EDGE_CURVE ( 'NONE', #2461, #586, #1441, .T. ) ;
#4012=CIRCLE ( 'NONE', #5120, 2.000000000000000000 ) ;
#4058=FACE_OUTER_BOUND ( 'NONE', #757, .T. ) ;
#4078=VECTOR ( 'NONE', #5297, 1000.000000000000000 ) ;
#4079=ORIENTED_EDGE ( 'NONE', *, *, #4790, .F. ) ;
#4081=AXIS2_PLACEMENT_3D ( 'NONE', #2744, #4434, #3630 ) ;
#4089=DIRECTION ( 'NONE',  ( -0.000000000000000000, -0.000000000000000000, 1.000000000000000000 ) ) ;
#4095=FACE_OUTER_BOUND ( 'NONE', #171, .T. ) ;
#4096=VERTEX_POINT ( 'NONE', #516 ) ;
#4097=AXIS2_PLACEMENT_3D ( 'NONE', #4615, #1569, #2889 ) ;
#4108=AXIS2_PLACEMENT_3D ( 'NONE', #2966, #725, #2129 ) ;
#4115=DIRECTION ( 'NONE',  ( -0.8571673007021134438, 1.049727191138619928E-16, 0.5150380749100523792 ) ) ;
#4119=AXIS2_PLACEMENT_3D ( 'NONE', #662, #4089, #1985 ) ;
#4125=ORIENTED_EDGE ( 'NONE', *, *, #1454, .T. ) ;
#4144=LINE ( 'NONE', #1952, #3837 ) ;
#4148=LINE ( 'NONE', #4579, #4994 ) ;
#4154=EDGE_CURVE ( 'NONE', #4844, #3499, #4632, .T. ) ;
#4174=FACE_OUTER_BOUND ( 'NONE', #4722, .T. ) ;
#4180=DIRECTION ( 'NONE',  ( -1.000000000000000000, 0.000000000000000000, -0.000000000000000000 ) ) ;
#4188=ORIENTED_EDGE ( 'NONE', *, *, #2557, .T. ) ;
#4194=ADVANCED_FACE ( 'NONE', ( #5508 ), #2458, .F. ) ;
#4195=AXIS2_PLACEMENT_3D ( 'NONE', #3409, #842, #5566 ) ;
#4197=ORIENTED_EDGE ( 'NONE', *, *, #3321, .F. ) ;
#4198=CIRCLE ( 'NONE', #2346, 23.00000000000000000 ) ;
#4206=AXIS2_PLACEMENT_3D ( 'NONE', #4725, #4275, #2489 ) ;
#4211=CYLINDRICAL_SURFACE ( 'NONE', #4470, 2.000000000000000000 ) ;
#4225=ORIENTED_EDGE ( 'NONE', *, *, #1278, .F. ) ;
#4242=CARTESIAN_POINT ( 'NONE',  ( 23.00000000000000000, 2.816687638038912352E-15, 2.000000000000000000 ) ) ;
#4244=DIRECTION ( 'NONE',  ( 0.000000000000000000, 0.000000000000000000, -1.000000000000000000 ) ) ;
#4270=VERTEX_POINT ( 'NONE', #756 ) ;
#4272=CARTESIAN_POINT ( 'NONE',  ( 17.99999999999999289, -15.01665741768121443, 8.000000000000000000 ) ) ;
#4275=DIRECTION ( 'NONE',  ( 0.000000000000000000, 0.000000000000000000, 1.000000000000000000 ) ) ;
#4279=( GEOMETRIC_REPRESENTATION_CONTEXT ( 3 ) GLOBAL_UNCERTAINTY_ASSIGNED_CONTEXT ( ( #3771 ) ) GLOBAL_UNIT_ASSIGNED_CONTEXT ( ( #1268, #2934, #5095 ) ) REPRESENTATION_CONTEXT ( 'NONE', 'WORKASPACE' ) );
#4284=DIRECTION ( 'NONE',  ( -0.000000000000000000, -0.000000000000000000, -1.000000000000000000 ) ) ;
#4289=AXIS2_PLACEMENT_3D ( 'NONE', #1907, #2856, #1992 ) ;
#4294=DIRECTION ( 'NONE',  ( -1.000000000000000000, 0.000000000000000000, 0.000000000000000000 ) ) ;
#4298=VECTOR ( 'NONE', #5551, 1000.000000000000000 ) ;
#4303=VERTEX_POINT ( 'NONE', #2025 ) ;
#4312=EDGE_CURVE ( 'NONE', #4732, #586, #2884, .T. ) ;
#4318=FACE_OUTER_BOUND ( 'NONE', #362, .T. ) ;
#4321=DIRECTION ( 'NONE',  ( -1.000000000000000000, 0.000000000000000000, 0.000000000000000000 ) ) ;
#4325=CARTESIAN_POINT ( 'NONE',  ( 0.000000000000000000, 0.000000000000000000, 0.000000000000000000 ) ) ;
#4334=DIRECTION ( 'NONE',  ( 1.000000000000000000, 0.000000000000000000, 0.000000000000000000 ) ) ;
#4353=AXIS2_PLACEMENT_3D ( 'NONE', #1103, #4613, #815 ) ;
#4354=PLANE ( 'NONE',  #769 ) ;
#4355=ORIENTED_EDGE ( 'NONE', *, *, #916, .F. ) ;
#4366=EDGE_LOOP ( 'NONE', ( #5430, #4904, #4622, #4411, #4437, #3454, #5032, #99 ) ) ;
#4368=VECTOR ( 'NONE', #5492, 1000.000000000000000 ) ;
#4372=VECTOR ( 'NONE', #915, 1000.000000000000000 ) ;
#4379=ORIENTED_EDGE ( 'NONE', *, *, #6, .F. ) ;
#4386=DIRECTION ( 'NONE',  ( 0.000000000000000000, 0.000000000000000000, 1.000000000000000000 ) ) ;
#4393=CIRCLE ( 'NONE', #5127, 23.00000000000000000 ) ;
#4404=ORIENTED_EDGE ( 'NONE', *, *, #1716, .F. ) ;
#4409=CARTESIAN_POINT ( 'NONE',  ( 0.000000000000000000, 0.000000000000000000, 0.000000000000000000 ) ) ;
#4411=ORIENTED_EDGE ( 'NONE', *, *, #2557, .F. ) ;
#4426=DIRECTION ( 'NONE',  ( -4.364351673553916694E-15, 1.000000000000000000, 0.000000000000000000 ) ) ;
#4430=ORIENTED_EDGE ( 'NONE', *, *, #3814, .T. ) ;
#4432=( NAMED_UNIT ( * ) SI_UNIT ( $, .STERADIAN. ) SOLID_ANGLE_UNIT ( ) );
#4434=DIRECTION ( 'NONE',  ( 0.000000000000000000, 0.000000000000000000, 1.000000000000000000 ) ) ;
#4437=ORIENTED_EDGE ( 'NONE', *, *, #3881, .F. ) ;
#4438=ORIENTED_EDGE ( 'NONE', *, *, #4154, .T. ) ;
#4458=DIRECTION ( 'NONE',  ( 0.8571673007021134438, 0.000000000000000000, 0.5150380749100523792 ) ) ;
#4459=ORIENTED_EDGE ( 'NONE', *, *, #4980, .T. ) ;
#4460=CARTESIAN_POINT ( 'NONE',  ( 4.999999999999923617, 22.44994432064366308, 5.000000000000000000 ) ) ;
#4465=FACE_OUTER_BOUND ( 'NONE', #3711, .T. ) ;
#4470=AXIS2_PLACEMENT_3D ( 'NONE', #262, #3775, #1474 ) ;
#4479=AXIS2_PLACEMENT_3D ( 'NONE', #229, #5385, #173 ) ;
#4484=ADVANCED_FACE ( 'NONE', ( #2276 ), #4354, .T. ) ;
#4488=VERTEX_POINT ( 'NONE', #5357 ) ;
#4490=CARTESIAN_POINT ( 'NONE',  ( 0.000000000000000000, 0.000000000000000000, 8.000000000000000000 ) ) ;
#4491=CARTESIAN_POINT ( 'NONE',  ( 0.000000000000000000, 0.000000000000000000, 8.000000000000000000 ) ) ;
#4495=DIRECTION ( 'NONE',  ( 1.000000000000000000, 0.000000000000000000, -0.000000000000000000 ) ) ;
#4513=EDGE_CURVE ( 'NONE', #1194, #132, #1970, .T. ) ;
#4518=CARTESIAN_POINT ( 'NONE',  ( -23.00000000000000000, 0.000000000000000000, 8.000000000000000000 ) ) ;
#4520=( NAMED_UNIT ( * ) PLANE_ANGLE_UNIT ( ) SI_UNIT ( $, .RADIAN. ) );
#4522=DIRECTION ( 'NONE',  ( 1.000000000000000000, 0.000000000000000000, 0.000000000000000000 ) ) ;
#4537=ORIENTED_EDGE ( 'NONE', *, *, #1524, .T. ) ;
#4539=AXIS2_PLACEMENT_3D ( 'NONE', #2157, #3028, #3054 ) ;
#4544=VECTOR ( 'NONE', #3284, 1000.000000000000000 ) ;
#4549=CIRCLE ( 'NONE', #4003, 25.00000000000000000 ) ;
#4553=VECTOR ( 'NONE', #3425, 1000.000000000000000 ) ;
#4556=CARTESIAN_POINT ( 'NONE',  ( -5.000000000000076383, 22.44994432064363110, 8.000000000000000000 ) ) ;
#4563=AXIS2_PLACEMENT_3D ( 'NONE', #2053, #4244, #1656 ) ;
#4568=DIRECTION ( 'NONE',  ( -3.540989467475305966E-16, -1.000000000000000000, 0.000000000000000000 ) ) ;
#4578=EDGE_CURVE ( 'NONE', #3011, #30, #3901, .T. ) ;
#4579=CARTESIAN_POINT ( 'NONE',  ( 22.99999999999999645, -8.485281374238580199, 8.000000000000000000 ) ) ;
#4580=CARTESIAN_POINT ( 'NONE',  ( 25.00000000000000000, 3.061616997868383043E-15, 8.000000000000000000 ) ) ;
#4585=EDGE_CURVE ( 'NONE', #4844, #2131, #576, .T. ) ;
#4590=CARTESIAN_POINT ( 'NONE',  ( -25.00000000000000000, 0.000000000000000000, 0.000000000000000000 ) ) ;
#4601=ORIENTED_EDGE ( 'NONE', *, *, #3071, .T. ) ;
#4606=EDGE_CURVE ( 'NONE', #5617, #5155, #4148, .T. ) ;
#4613=DIRECTION ( 'NONE',  ( 0.000000000000000000, 0.000000000000000000, 1.000000000000000000 ) ) ;
#4615=CARTESIAN_POINT ( 'NONE',  ( 0.000000000000000000, 0.000000000000000000, 2.000000000000000000 ) ) ;
#4622=ORIENTED_EDGE ( 'NONE', *, *, #2567, .T. ) ;
#4632=CIRCLE ( 'NONE', #4714, 25.00000000000000000 ) ;
#4636=CARTESIAN_POINT ( 'NONE',  ( 0.000000000000000000, 0.000000000000000000, 8.000000000000000000 ) ) ;
#4650=ORIENTED_EDGE ( 'NONE', *, *, #3227, .T. ) ;
#4659=CARTESIAN_POINT ( 'NONE',  ( 4.999999999999914735, 24.49489742783179835, 5.000000000000000000 ) ) ;
#4684=DIRECTION ( 'NONE',  ( -0.000000000000000000, -0.000000000000000000, -1.000000000000000000 ) ) ;
#4690=ORIENTED_EDGE ( 'NONE', *, *, #5077, .T. ) ;
#4696=EDGE_CURVE ( 'NONE', #2946, #4270, #3625, .T. ) ;
#4700=DIRECTION ( 'NONE',  ( -4.364351673553916694E-15, 1.000000000000000000, 0.000000000000000000 ) ) ;
#4706=FACE_OUTER_BOUND ( 'NONE', #3093, .T. ) ;
#4714=AXIS2_PLACEMENT_3D ( 'NONE', #2702, #3914, #5668 ) ;
#4717=FACE_OUTER_BOUND ( 'NONE', #3655, .T. ) ;
#4719=AXIS2_PLACEMENT_3D ( 'NONE', #523, #1010, #2303 ) ;
#4722=EDGE_LOOP ( 'NONE', ( #3376, #2820 ) ) ;
#4725=CARTESIAN_POINT ( 'NONE',  ( 0.000000000000000000, 0.000000000000000000, 2.000000000000000000 ) ) ;
#4729=AXIS2_PLACEMENT_3D ( 'NONE', #1404, #3457, #374 ) ;
#4732=VERTEX_POINT ( 'NONE', #2982 ) ;
#4741=AXIS2_PLACEMENT_3D ( 'NONE', #5612, #1673, #5181 ) ;
#4742=SURFACE_STYLE_USAGE ( .BOTH. , #1210 ) ;
#4744=VECTOR ( 'NONE', #3694, 1000.000000000000000 ) ;
#4745=CYLINDRICAL_SURFACE ( 'NONE', #5295, 23.00000000000000000 ) ;
#4747=ORIENTED_EDGE ( 'NONE', *, *, #4606, .F. ) ;
#4753=ORIENTED_EDGE ( 'NONE', *, *, #4696, .F. ) ;
#4754=CARTESIAN_POINT ( 'NONE',  ( -5.000000000000085265, 24.49489742783176638, 8.000000000000000000 ) ) ;
#4766=EDGE_CURVE ( 'NONE', #586, #4732, #5553, .T. ) ;
#4773=DIRECTION ( 'NONE',  ( 0.000000000000000000, 0.000000000000000000, -1.000000000000000000 ) ) ;
#4790=EDGE_CURVE ( 'NONE', #1000, #1733, #5374, .T. ) ;
#4791=ORIENTED_EDGE ( 'NONE', *, *, #2567, .F. ) ;
#4809=ORIENTED_EDGE ( 'NONE', *, *, #1864, .T. ) ;
#4815=FACE_OUTER_BOUND ( 'NONE', #1708, .T. ) ;
#4825=ADVANCED_FACE ( 'NONE', ( #4815 ), #1288, .T. ) ;
#4843=ADVANCED_FACE ( 'NONE', ( #944 ), #3139, .F. ) ;
#4844=VERTEX_POINT ( 'NONE', #2617 ) ;
#4851=VERTEX_POINT ( 'NONE', #2214 ) ;
#4860=LINE ( 'NONE', #943, #4372 ) ;
#4892=DIRECTION ( 'NONE',  ( 0.000000000000000000, 0.000000000000000000, 1.000000000000000000 ) ) ;
#4896=CARTESIAN_POINT ( 'NONE',  ( 18.00000000000000000, 1.553654299240552096E-15, 8.000000000000000000 ) ) ;
#4897=ORIENTED_EDGE ( 'NONE', *, *, #1211, .T. ) ;
#4904=ORIENTED_EDGE ( 'NONE', *, *, #1927, .T. ) ;
#4920=CARTESIAN_POINT ( 'NONE',  ( 2.000000000000000000, 0.000000000000000000, 4.000000000000000000 ) ) ;
#4923=CARTESIAN_POINT ( 'NONE',  ( 0.000000000000000000, 0.000000000000000000, 8.000000000000000000 ) ) ;
#4924=EDGE_CURVE ( 'NONE', #4096, #525, #2156, .T. ) ;
#4927=ORIENTED_EDGE ( 'NONE', *, *, #3014, .T. ) ;
#4931=STYLED_ITEM('',(#5737),#652);
#4935=ORIENTED_EDGE ( 'NONE', *, *, #5183, .T. ) ;
#4950=CARTESIAN_POINT ( 'NONE',  ( 23.24999999999999645, -8.485281374238580199, 4.000000000000000000 ) ) ;
#4955=ORIENTED_EDGE ( 'NONE', *, *, #3022, .T. ) ;
#4972=LINE ( 'NONE', #111, #5584 ) ;
#4980=EDGE_CURVE ( 'NONE', #525, #1733, #1298, .T. ) ;
#4985=ORIENTED_EDGE ( 'NONE', *, *, #5029, .F. ) ;
#4994=VECTOR ( 'NONE', #3256, 1000.000000000000000 ) ;
#5000=VECTOR ( 'NONE', #4568, 1000.000000000000000 ) ;
#5003=AXIS2_PLACEMENT_3D ( 'NONE', #3859, #3886, #5179 ) ;
#5004=STYLED_ITEM ( 'NONE', ( #2476 ), #69 ) ;
#5010=AXIS2_PLACEMENT_3D ( 'NONE', #4409, #927, #35 ) ;
#5029=EDGE_CURVE ( 'NONE', #2459, #5617, #945, .T. ) ;
#5032=ORIENTED_EDGE ( 'NONE', *, *, #4790, .T. ) ;
#5038=ORIENTED_EDGE ( 'NONE', *, *, #81, .F. ) ;
#5061=DIRECTION ( 'NONE',  ( 0.000000000000000000, 0.000000000000000000, 1.000000000000000000 ) ) ;
#5066=FACE_OUTER_BOUND ( 'NONE', #192, .T. ) ;
#5071=ORIENTED_EDGE ( 'NONE', *, *, #1454, .F. ) ;
#5077=EDGE_CURVE ( 'NONE', #993, #92, #1437, .T. ) ;
#5083=ORIENTED_EDGE ( 'NONE', *, *, #155, .T. ) ;
#5089=ORIENTED_EDGE ( 'NONE', *, *, #2928, .F. ) ;
#5095=( NAMED_UNIT ( * ) SI_UNIT ( $, .STERADIAN. ) SOLID_ANGLE_UNIT ( ) );
#5097=DIRECTION ( 'NONE',  ( 1.000000000000000000, 0.000000000000000000, 0.000000000000000000 ) ) ;
#5102=CIRCLE ( 'NONE', #135, 0.2500000000000002220 ) ;
#5120=AXIS2_PLACEMENT_3D ( 'NONE', #2503, #5558, #3346 ) ;
#5127=AXIS2_PLACEMENT_3D ( 'NONE', #1782, #3482, #2624 ) ;
#5128=CARTESIAN_POINT ( 'NONE',  ( 0.000000000000000000, 0.000000000000000000, 8.000000000000000000 ) ) ;
#5132=DIRECTION ( 'NONE',  ( -1.000000000000000000, 0.000000000000000000, 0.000000000000000000 ) ) ;
#5138=ORIENTED_EDGE ( 'NONE', *, *, #4766, .T. ) ;
#5139=FACE_BOUND ( 'NONE', #3150, .T. ) ;
#5145=PRODUCT ( 'outer cover 1', 'outer cover 1', '', ( #2693 ) ) ;
#5155=VERTEX_POINT ( 'NONE', #2734 ) ;
#5162=ORIENTED_EDGE ( 'NONE', *, *, #1380, .T. ) ;
#5179=DIRECTION ( 'NONE',  ( 1.000000000000000000, 0.000000000000000000, 0.000000000000000000 ) ) ;
#5181=DIRECTION ( 'NONE',  ( -1.000000000000000000, 0.000000000000000000, 0.000000000000000000 ) ) ;
#5183=EDGE_CURVE ( 'NONE', #3426, #3736, #2761, .T. ) ;
#5188=ORIENTED_EDGE ( 'NONE', *, *, #925, .T. ) ;
#5190=ORIENTED_EDGE ( 'NONE', *, *, #1872, .F. ) ;
#5213=DIRECTION ( 'NONE',  ( 1.000000000000000000, 0.000000000000000000, 0.000000000000000000 ) ) ;
#5216=CARTESIAN_POINT ( 'NONE',  ( 0.000000000000000000, 0.000000000000000000, 8.000000000000000000 ) ) ;
#5219=DIRECTION ( 'NONE',  ( -0.000000000000000000, -0.000000000000000000, -1.000000000000000000 ) ) ;
#5225=LINE ( 'NONE', #4754, #877 ) ;
#5227=LINE ( 'NONE', #1739, #1723 ) ;
#5247=( LENGTH_UNIT ( ) NAMED_UNIT ( * ) SI_UNIT ( .MILLI., .METRE. ) );
#5256=CARTESIAN_POINT ( 'NONE',  ( 0.000000000000000000, 0.000000000000000000, 2.000000000000000000 ) ) ;
#5265=CARTESIAN_POINT ( 'NONE',  ( 0.000000000000000000, 0.000000000000000000, 5.000000000000000000 ) ) ;
#5268=EDGE_CURVE ( 'NONE', #2258, #4732, #3335, .T. ) ;
#5271=ORIENTED_EDGE ( 'NONE', *, *, #2632, .F. ) ;
#5276=ORIENTED_EDGE ( 'NONE', *, *, #4924, .T. ) ;
#5277=FACE_OUTER_BOUND ( 'NONE', #3679, .T. ) ;
#5295=AXIS2_PLACEMENT_3D ( 'NONE', #5216, #400, #4321 ) ;
#5297=DIRECTION ( 'NONE',  ( -0.000000000000000000, -0.000000000000000000, -1.000000000000000000 ) ) ;
#5304=AXIS2_PLACEMENT_3D ( 'NONE', #3300, #2004, #1595 ) ;
#5319=SHAPE_DEFINITION_REPRESENTATION ( #2426, #3487 ) ;
#5325=CARTESIAN_POINT ( 'NONE',  ( -5.000000000000000000, 0.000000000000000000, 8.000000000000000000 ) ) ;
#5327=ORIENTED_EDGE ( 'NONE', *, *, #5662, .T. ) ;
#5357=CARTESIAN_POINT ( 'NONE',  ( -5.000000000000076383, 22.44994432064363110, 8.000000000000000000 ) ) ;
#5358=DIRECTION ( 'NONE',  ( 0.000000000000000000, 0.000000000000000000, 1.000000000000000000 ) ) ;
#5374=CIRCLE ( 'NONE', #2704, 25.00000000000000000 ) ;
#5385=DIRECTION ( 'NONE',  ( 0.000000000000000000, 0.000000000000000000, 1.000000000000000000 ) ) ;
#5388=( LENGTH_UNIT ( ) NAMED_UNIT ( * ) SI_UNIT ( .MILLI., .METRE. ) );
#5397=VERTEX_POINT ( 'NONE', #2011 ) ;
#5398=AXIS2_PLACEMENT_3D ( 'NONE', #1386, #3969, #402 ) ;
#5404=ORIENTED_EDGE ( 'NONE', *, *, #5546, .T. ) ;
#5418=DIRECTION ( 'NONE',  ( -0.000000000000000000, -0.000000000000000000, 1.000000000000000000 ) ) ;
#5430=ORIENTED_EDGE ( 'NONE', *, *, #3227, .F. ) ;
#5439=DIRECTION ( 'NONE',  ( 0.000000000000000000, 0.000000000000000000, 1.000000000000000000 ) ) ;
#5463=ADVANCED_FACE ( 'NONE', ( #4706 ), #768, .T. ) ;
#5467=PLANE ( 'NONE',  #990 ) ;
#5483=LINE ( 'NONE', #2340, #4744 ) ;
#5492=DIRECTION ( 'NONE',  ( -0.000000000000000000, -0.000000000000000000, -1.000000000000000000 ) ) ;
#5495=CIRCLE ( 'NONE', #1270, 23.00000000000000000 ) ;
#5508=FACE_OUTER_BOUND ( 'NONE', #870, .T. ) ;
#5512=CARTESIAN_POINT ( 'NONE',  ( 0.000000000000000000, 0.000000000000000000, 2.798278761944885229 ) ) ;
#5525=APPLICATION_CONTEXT ( 'automotive_design' ) ;
#5530=FACE_OUTER_BOUND ( 'NONE', #1132, .T. ) ;
#5544=VERTEX_POINT ( 'NONE', #954 ) ;
#5546=EDGE_CURVE ( 'NONE', #2459, #5397, #522, .T. ) ;
#5551=DIRECTION ( 'NONE',  ( 0.000000000000000000, 0.000000000000000000, 1.000000000000000000 ) ) ;
#5553=CIRCLE ( 'NONE', #1142, 5.000000000000000000 ) ;
#5558=DIRECTION ( 'NONE',  ( -0.000000000000000000, -0.000000000000000000, 1.000000000000000000 ) ) ;
#5565=ORIENTED_EDGE ( 'NONE', *, *, #5029, .T. ) ;
#5566=DIRECTION ( 'NONE',  ( -1.000000000000000000, 0.000000000000000000, 0.000000000000000000 ) ) ;
#5573=ORIENTED_EDGE ( 'NONE', *, *, #4011, .F. ) ;
#5584=VECTOR ( 'NONE', #141, 1000.000000000000000 ) ;
#5585=DIRECTION ( 'NONE',  ( 1.000000000000000000, 0.000000000000000000, 0.000000000000000000 ) ) ;
#5590=DIRECTION ( 'NONE',  ( 0.000000000000000000, 0.000000000000000000, 1.000000000000000000 ) ) ;
#5595=VERTEX_POINT ( 'NONE', #2448 ) ;
#5612=CARTESIAN_POINT ( 'NONE',  ( 0.000000000000000000, 0.000000000000000000, 8.000000000000000000 ) ) ;
#5617=VERTEX_POINT ( 'NONE', #3629 ) ;
#5628=LINE ( 'NONE', #1376, #1818 ) ;
#5634=CARTESIAN_POINT ( 'NONE',  ( 23.24999999999999645, -8.485281374238580199, 8.000000000000000000 ) ) ;
#5643=AXIS2_PLACEMENT_3D ( 'NONE', #3208, #180, #2363 ) ;
#5650=CARTESIAN_POINT ( 'NONE',  ( -2.000000000000000000, 2.449293598294706414E-16, 8.000000000000000000 ) ) ;
#5662=EDGE_CURVE ( 'NONE', #4851, #5544, #5102, .T. ) ;
#5667=DIRECTION ( 'NONE',  ( -3.540989467475305966E-16, -1.000000000000000000, 0.000000000000000000 ) ) ;
#5668=DIRECTION ( 'NONE',  ( 1.000000000000000000, 0.000000000000000000, 0.000000000000000000 ) ) ;
#5680=EDGE_LOOP ( 'NONE', ( #3573, #109 ) ) ;
#5684=DIRECTION ( 'NONE',  ( 1.000000000000000000, 4.364351673553916694E-15, 0.000000000000000000 ) ) ;
#5687=DIRECTION ( 'NONE',  ( -0.000000000000000000, -0.000000000000000000, -1.000000000000000000 ) ) ;
#5731=COLOUR_RGB('Off White',0.89,0.88,0.83);
#5732=FILL_AREA_STYLE_COLOUR('',#5731);
#5733=FILL_AREA_STYLE('',(#5732));
#5734=SURFACE_STYLE_FILL_AREA(#5733);
#5735=SURFACE_SIDE_STYLE('',(#5734));
#5736=SURFACE_STYLE_USAGE(.BOTH.,#5735);
#5737=PRESENTATION_STYLE_ASSIGNMENT((#5736));
ENDSEC;
END-ISO-10303-21;
